ISO-10303-21;
HEADER;
FILE_DESCRIPTION (('STEP AP214'),
    '1' );
FILE_NAME ('Rivet.step',
    '2026-10-06T09:00:30',
    ( '' ),
    ( '' ),
    'SwSTEP 2.0',
    'SolidWorks 2020',
    '' );
FILE_SCHEMA (( 'AUTOMOTIVE_DESIGN' ));
ENDSEC;

DATA;
#74=CARTESIAN_POINT ( 'NONE',  ( 15.69372571266449512, 10.97998838177520931, -1.972246272986471594 ) ) ;
#287=ADVANCED_FACE ( 'NONE', ( #20132 ), #22799, .T. ) ;
#297=ORIENTED_EDGE ( 'NONE', *, *, #4833, .F. ) ;
#527=SHAPE_REPRESENTATION ( 'Rivet', ( #17722 ), #2272 ) ;
#565=VERTEX_POINT ( 'NONE', #8271 ) ;
#574=UNCERTAINTY_MEASURE_WITH_UNIT (LENGTH_MEASURE( 1.000000000000000082E-05 ), #26475, 'distance_accuracy_value', 'NONE');
#649=CIRCLE ( 'NONE', #8157, 1.472846691535505848 ) ;
#881=DIRECTION ( 'NONE',  ( -0.000000000000000000, -0.000000000000000000, -1.000000000000000000 ) ) ;
#943=APPLICATION_CONTEXT ( 'automotive_design' ) ;
#1076=CARTESIAN_POINT ( 'NONE',  ( 17.16657240420000008, 12.63606054916536614, 0.05106179917585308009 ) ) ;
#1246=ORIENTED_EDGE ( 'NONE', *, *, #28669, .T. ) ;
#1585=CARTESIAN_POINT ( 'NONE',  ( 18.28639557936419280, 10.97998838177520931, 0.05106179917585291356 ) ) ;
#1693=DIRECTION ( 'NONE',  ( 0.3326278240906416217, 0.000000000000000000, 0.9430581798811381589 ) ) ;
#2213=FACE_OUTER_BOUND ( 'NONE', #18410, .T. ) ;
#2272=( GEOMETRIC_REPRESENTATION_CONTEXT ( 3 ) GLOBAL_UNCERTAINTY_ASSIGNED_CONTEXT ( ( #574 ) ) GLOBAL_UNIT_ASSIGNED_CONTEXT ( ( #26475, #6972, #21757 ) ) REPRESENTATION_CONTEXT ( 'NONE', 'WORKASPACE' ) );
#2498=DIRECTION ( 'NONE',  ( 0.000000000000000000, 0.000000000000000000, 1.000000000000000000 ) ) ;
#2512=DIRECTION ( 'NONE',  ( 0.000000000000000000, 0.000000000000000000, 1.000000000000000000 ) ) ;
#2543=DIRECTION ( 'NONE',  ( -1.000000000000000000, 0.000000000000000000, 0.000000000000000000 ) ) ;
#2590=CARTESIAN_POINT ( 'NONE',  ( 15.51050023680984680, 10.97998838177520931, 0.05106179917585291356 ) ) ;
#2627=CARTESIAN_POINT ( 'NONE',  ( 0.000000000000000000, 0.000000000000000000, 0.000000000000000000 ) ) ;
#2722=AXIS2_PLACEMENT_3D ( 'NONE', #8150, #17745, #22341 ) ;
#2763=AXIS2_PLACEMENT_3D ( 'NONE', #1076, #19810, #3115 ) ;
#2798=DIRECTION ( 'NONE',  ( 0.000000000000000000, 0.000000000000000000, 1.000000000000000000 ) ) ;
#2932=CARTESIAN_POINT ( 'NONE',  ( 15.69372571266449512, 10.97998838177520931, 0.5194763363741546902 ) ) ;
#3115=DIRECTION ( 'NONE',  ( -1.000000000000000000, 0.000000000000000000, 0.000000000000000000 ) ) ;
#3200=AXIS2_PLACEMENT_3D ( 'NONE', #29742, #27384, #20150 ) ;
#3222=VECTOR ( 'NONE', #15689, 1000.000000000000114 ) ;
#3346=EDGE_CURVE ( 'NONE', #24961, #5834, #13024, .T. ) ;
#3422=FACE_BOUND ( 'NONE', #21721, .T. ) ;
#3653=AXIS2_PLACEMENT_3D ( 'NONE', #28552, #7308, #19108 ) ;
#3823=ORIENTED_EDGE ( 'NONE', *, *, #14624, .T. ) ;
#3917=FILL_AREA_STYLE ('',( #30189 ) ) ;
#4013=CLOSED_SHELL ( 'NONE', ( #25105, #21530, #17356, #7305, #29201, #22181, #11554, #12812, #287, #11912 ) ) ;
#4016=DIRECTION ( 'NONE',  ( -0.000000000000000000, -0.000000000000000000, -1.000000000000000000 ) ) ;
#4142=EDGE_LOOP ( 'NONE', ( #4413, #14991, #5800, #22104 ) ) ;
#4331=DIRECTION ( 'NONE',  ( -1.000000000000000000, 0.000000000000000000, 0.000000000000000000 ) ) ;
#4413=ORIENTED_EDGE ( 'NONE', *, *, #28364, .F. ) ;
#4486=DIRECTION ( 'NONE',  ( -1.000000000000000000, 0.000000000000000000, 0.000000000000000000 ) ) ;
#4489=DIRECTION ( 'NONE',  ( -0.000000000000000000, -0.000000000000000000, -1.000000000000000000 ) ) ;
#4604=SURFACE_STYLE_FILL_AREA ( #26781 ) ;
#4642=ORIENTED_EDGE ( 'NONE', *, *, #26958, .T. ) ;
#4720=DIRECTION ( 'NONE',  ( -1.000000000000000000, 0.000000000000000000, 0.000000000000000000 ) ) ;
#4741=EDGE_CURVE ( 'NONE', #24961, #5868, #18151, .T. ) ;
#4832=CARTESIAN_POINT ( 'NONE',  ( 17.16657240420000008, 10.97998838177520931, -1.972246272986471594 ) ) ;
#4833=EDGE_CURVE ( 'NONE', #10669, #15475, #26645, .T. ) ;
#5239=DIRECTION ( 'NONE',  ( -0.3326278240906416217, 4.073516000799531462E-17, 0.9430581798811381589 ) ) ;
#5247=DIRECTION ( 'NONE',  ( -1.000000000000000000, 0.000000000000000000, 0.000000000000000000 ) ) ;
#5316=FACE_OUTER_BOUND ( 'NONE', #28028, .T. ) ;
#5440=DIRECTION ( 'NONE',  ( -0.000000000000000000, -0.000000000000000000, -1.000000000000000000 ) ) ;
#5446=AXIS2_PLACEMENT_3D ( 'NONE', #21532, #2798, #16953 ) ;
#5489=ORIENTED_EDGE ( 'NONE', *, *, #14624, .F. ) ;
#5659=CARTESIAN_POINT ( 'NONE',  ( 15.51050023680984502, 10.97998838177520931, -1.452769935612311825 ) ) ;
#5800=ORIENTED_EDGE ( 'NONE', *, *, #9438, .T. ) ;
#5834=VERTEX_POINT ( 'NONE', #23837 ) ;
#5868=VERTEX_POINT ( 'NONE', #12475 ) ;
#5899=STYLED_ITEM ( 'NONE', ( #19168 ), #11026 ) ;
#5925=LINE ( 'NONE', #22934, #27556 ) ;
#5935=CONICAL_SURFACE ( 'NONE', #5446, 1.472846691535505848, 0.3390887027916915653 ) ;
#5939=FACE_OUTER_BOUND ( 'NONE', #10917, .T. ) ;
#6261=AXIS2_PLACEMENT_3D ( 'NONE', #14325, #2512, #12250 ) ;
#6275=STYLED_ITEM ( 'NONE', ( #14374 ), #21175 ) ;
#6518=CARTESIAN_POINT ( 'NONE',  ( 18.28658402242479397, 10.97998838177520931, -1.452769935612311825 ) ) ;
#6612=ORIENTED_EDGE ( 'NONE', *, *, #20386, .T. ) ;
#6643=EDGE_LOOP ( 'NONE', ( #25826, #25096, #22427, #14606 ) ) ;
#6972=( NAMED_UNIT ( * ) PLANE_ANGLE_UNIT ( ) SI_UNIT ( $, .RADIAN. ) );
#7292=( GEOMETRIC_REPRESENTATION_CONTEXT ( 3 ) GLOBAL_UNCERTAINTY_ASSIGNED_CONTEXT ( ( #19755 ) ) GLOBAL_UNIT_ASSIGNED_CONTEXT ( ( #17783, #29604, #17934 ) ) REPRESENTATION_CONTEXT ( 'NONE', 'WORKASPACE' ) );
#7305=ADVANCED_FACE ( 'NONE', ( #7625, #14883 ), #9842, .T. ) ;
#7308=DIRECTION ( 'NONE',  ( -0.000000000000000000, -0.000000000000000000, -1.000000000000000000 ) ) ;
#7363=( LENGTH_UNIT ( ) NAMED_UNIT ( * ) SI_UNIT ( .MILLI., .METRE. ) );
#7415=MECHANICAL_DESIGN_GEOMETRIC_PRESENTATION_REPRESENTATION('',(#5899),#18465);
#7441=AXIS2_PLACEMENT_3D ( 'NONE', #26803, #10130, #5247 ) ;
#7625=FACE_BOUND ( 'NONE', #22568, .T. ) ;
#7735=AXIS2_PLACEMENT_3D ( 'NONE', #29194, #22599, #22129 ) ;
#7919=CARTESIAN_POINT ( 'NONE',  ( 17.16657240420000008, 10.97998838177520931, -1.452769935612311825 ) ) ;
#8150=CARTESIAN_POINT ( 'NONE',  ( 17.16657240420000008, 12.45283507331071426, -1.972246272986471594 ) ) ;
#8157=AXIS2_PLACEMENT_3D ( 'NONE', #4832, #28735, #28590 ) ;
#8246=DIRECTION ( 'NONE',  ( -1.000000000000000000, 0.000000000000000000, 0.000000000000000000 ) ) ;
#8271=CARTESIAN_POINT ( 'NONE',  ( 18.63941909573550859, 10.97998838177520931, -1.972246272986471594 ) ) ;
#8400=CARTESIAN_POINT ( 'NONE',  ( 17.16657240420000008, 10.97998838177520931, 0.05106179917585291356 ) ) ;
#8443=LINE ( 'NONE', #18043, #3222 ) ;
#8700=CIRCLE ( 'NONE', #15729, 1.119823175164191165 ) ;
#8822=CARTESIAN_POINT ( 'NONE',  ( 15.69372571266449512, 10.97998838177520931, -1.972246272986471594 ) ) ;
#8888=PRODUCT_DEFINITION_SHAPE ( 'NONE', 'NONE',  #22352 ) ;
#8952=CONICAL_SURFACE ( 'NONE', #23028, 1.656072167390155281, 0.3728633601815770082 ) ;
#9032=ORIENTED_EDGE ( 'NONE', *, *, #24083, .T. ) ;
#9247=SURFACE_STYLE_USAGE ( .BOTH. , #19479 ) ;
#9354=CARTESIAN_POINT ( 'NONE',  ( 17.16657240420000008, 10.97998838177520931, 0.5194763363741546902 ) ) ;
#9356=ORIENTED_EDGE ( 'NONE', *, *, #17106, .T. ) ;
#9438=EDGE_CURVE ( 'NONE', #15475, #22567, #15976, .T. ) ;
#9483=SURFACE_STYLE_USAGE ( .BOTH. , #14211 ) ;
#9509=DIRECTION ( 'NONE',  ( -0.000000000000000000, -0.000000000000000000, -1.000000000000000000 ) ) ;
#9642=DIRECTION ( 'NONE',  ( -0.0001253086065159677936, 0.000000000000000000, -0.9999999921488764709 ) ) ;
#9643=VECTOR ( 'NONE', #1693, 1000.000000000000000 ) ;
#9767=CONICAL_SURFACE ( 'NONE', #17283, 1.656072167390155281, 0.3728633601815770082 ) ;
#9842=PLANE ( 'NONE',  #27114 ) ;
#9911=VECTOR ( 'NONE', #9642, 1000.000000000000114 ) ;
#9932=CARTESIAN_POINT ( 'NONE',  ( 17.16657240420000008, 10.97998838177520931, -1.972246272986471594 ) ) ;
#10130=DIRECTION ( 'NONE',  ( -0.000000000000000000, -0.000000000000000000, -1.000000000000000000 ) ) ;
#10169=CARTESIAN_POINT ( 'NONE',  ( 17.16657240420000008, 10.97998838177520931, 0.05106179917585291356 ) ) ;
#10549=EDGE_CURVE ( 'NONE', #5834, #27894, #14533, .T. ) ;
#10556=FACE_OUTER_BOUND ( 'NONE', #6643, .T. ) ;
#10561=EDGE_LOOP ( 'NONE', ( #297, #21177, #15841, #6612 ) ) ;
#10620=CARTESIAN_POINT ( 'NONE',  ( 16.04656078597520974, 10.97998838177520931, -1.452769935612311825 ) ) ;
#10669=VERTEX_POINT ( 'NONE', #8822 ) ;
#10729=AXIS2_PLACEMENT_3D ( 'NONE', #9354, #31081, #28712 ) ;
#10771=ORIENTED_EDGE ( 'NONE', *, *, #3346, .F. ) ;
#10838=PRODUCT_DEFINITION_FORMATION_WITH_SPECIFIED_SOURCE ( 'ANY', '', #30511, .NOT_KNOWN. ) ;
#10917=EDGE_LOOP ( 'NONE', ( #26743, #9032 ) ) ;
#10997=EDGE_LOOP ( 'NONE', ( #12026, #14407 ) ) ;
#11026=MANIFOLD_SOLID_BREP ( 'Stock-MAS-156-1', #4013 ) ;
#11133=LINE ( 'NONE', #27964, #9643 ) ;
#11189=AXIS2_PLACEMENT_3D ( 'NONE', #11869, #9509, #4331 ) ;
#11354=DIRECTION ( 'NONE',  ( -1.000000000000000000, 0.000000000000000000, 0.000000000000000000 ) ) ;
#11420=ORIENTED_EDGE ( 'NONE', *, *, #29712, .T. ) ;
#11497=ORIENTED_EDGE ( 'NONE', *, *, #26958, .F. ) ;
#11554=ADVANCED_FACE ( 'NONE', ( #2213 ), #8952, .T. ) ;
#11800=CARTESIAN_POINT ( 'NONE',  ( 17.16657240420000008, 10.97998838177520931, 0.05106179917585291356 ) ) ;
#11869=CARTESIAN_POINT ( 'NONE',  ( 17.16657240420000008, 10.97998838177520931, 0.05106179917585291356 ) ) ;
#11912=ADVANCED_FACE ( 'NONE', ( #14609 ), #5935, .T. ) ;
#11952=CIRCLE ( 'NONE', #7441, 1.120011618224791450 ) ;
#12026=ORIENTED_EDGE ( 'NONE', *, *, #20386, .F. ) ;
#12233=( NAMED_UNIT ( * ) SI_UNIT ( $, .STERADIAN. ) SOLID_ANGLE_UNIT ( ) );
#12250=DIRECTION ( 'NONE',  ( 1.000000000000000000, 0.000000000000000000, 0.000000000000000000 ) ) ;
#12475=CARTESIAN_POINT ( 'NONE',  ( 18.28658402242479397, 10.97998838177520931, -1.452769935612311825 ) ) ;
#12812=ADVANCED_FACE ( 'NONE', ( #5316 ), #17266, .T. ) ;
#12924=SHAPE_REPRESENTATION_RELATIONSHIP ( 'NONE' , 'NONE' ,  #527, #21175 ) ;
#12987=FACE_OUTER_BOUND ( 'NONE', #13876, .T. ) ;
#13024=CIRCLE ( 'NONE', #25604, 1.119823175164191165 ) ;
#13325=DIRECTION ( 'NONE',  ( 0.3642835349036590564, 4.461186650018491474E-17, -0.9312880897971875793 ) ) ;
#13876=EDGE_LOOP ( 'NONE', ( #3823, #25783, #21996, #24272 ) ) ;
#14015=DIRECTION ( 'NONE',  ( 0.000000000000000000, 0.000000000000000000, 1.000000000000000000 ) ) ;
#14211=SURFACE_SIDE_STYLE ('',( #4604 ) ) ;
#14246=AXIS2_PLACEMENT_3D ( 'NONE', #9932, #26611, #2543 ) ;
#14325=CARTESIAN_POINT ( 'NONE',  ( 17.16657240420000008, 10.97998838177520931, -1.972246272986471594 ) ) ;
#14374=PRESENTATION_STYLE_ASSIGNMENT (( #9483 ) ) ;
#14407=ORIENTED_EDGE ( 'NONE', *, *, #9438, .F. ) ;
#14450=ORIENTED_EDGE ( 'NONE', *, *, #24083, .F. ) ;
#14533=LINE ( 'NONE', #21457, #9911 ) ;
#14606=ORIENTED_EDGE ( 'NONE', *, *, #15024, .F. ) ;
#14609=FACE_OUTER_BOUND ( 'NONE', #10561, .T. ) ;
#14624=EDGE_CURVE ( 'NONE', #22582, #23024, #15016, .T. ) ;
#14745=ORIENTED_EDGE ( 'NONE', *, *, #15024, .T. ) ;
#14883=FACE_OUTER_BOUND ( 'NONE', #10997, .T. ) ;
#14991=ORIENTED_EDGE ( 'NONE', *, *, #4833, .T. ) ;
#15016=CIRCLE ( 'NONE', #19053, 1.472846691535505848 ) ;
#15024=EDGE_CURVE ( 'NONE', #5868, #27894, #11952, .T. ) ;
#15097=SHAPE_DEFINITION_REPRESENTATION ( #8888, #527 ) ;
#15155=ORIENTED_EDGE ( 'NONE', *, *, #28364, .T. ) ;
#15475=VERTEX_POINT ( 'NONE', #5659 ) ;
#15689=DIRECTION ( 'NONE',  ( -0.3642835349036590564, 0.000000000000000000, -0.9312880897971875793 ) ) ;
#15729=AXIS2_PLACEMENT_3D ( 'NONE', #8400, #18000, #27451 ) ;
#15841=ORIENTED_EDGE ( 'NONE', *, *, #18887, .T. ) ;
#15941=EDGE_CURVE ( 'NONE', #23024, #19165, #5925, .T. ) ;
#15976=CIRCLE ( 'NONE', #27527, 1.656072167390155281 ) ;
#16115=DIRECTION ( 'NONE',  ( 0.0001253086065159677936, 1.534587838753951648E-20, -0.9999999921488764709 ) ) ;
#16436=FACE_OUTER_BOUND ( 'NONE', #24781, .T. ) ;
#16803=CARTESIAN_POINT ( 'NONE',  ( 17.16657240420000008, 10.97998838177520931, 0.5194763363741543571 ) ) ;
#16911=DIRECTION ( 'NONE',  ( 1.000000000000000000, 0.000000000000000000, -0.000000000000000000 ) ) ;
#16953=DIRECTION ( 'NONE',  ( 1.000000000000000000, 0.000000000000000000, 0.000000000000000000 ) ) ;
#17106=EDGE_CURVE ( 'NONE', #565, #10669, #649, .T. ) ;
#17210=ORIENTED_EDGE ( 'NONE', *, *, #15941, .F. ) ;
#17266=PLANE ( 'NONE',  #20543 ) ;
#17283=AXIS2_PLACEMENT_3D ( 'NONE', #10169, #5440, #22281 ) ;
#17356=ADVANCED_FACE ( 'NONE', ( #16436 ), #29285, .T. ) ;
#17377=EDGE_CURVE ( 'NONE', #30573, #19165, #19233, .T. ) ;
#17447=PRODUCT_CONTEXT ( 'NONE', #943, 'mechanical' ) ;
#17569=UNCERTAINTY_MEASURE_WITH_UNIT (LENGTH_MEASURE( 1.000000000000000082E-05 ), #7363, 'distance_accuracy_value', 'NONE');
#17685=CARTESIAN_POINT ( 'NONE',  ( 17.16657240420000008, 10.97998838177520931, 0.5194763363741546902 ) ) ;
#17722=AXIS2_PLACEMENT_3D ( 'NONE', #2627, #14015, #29203 ) ;
#17745=DIRECTION ( 'NONE',  ( -0.000000000000000000, 0.000000000000000000, -1.000000000000000000 ) ) ;
#17783=( LENGTH_UNIT ( ) NAMED_UNIT ( * ) SI_UNIT ( .MILLI., .METRE. ) );
#17789=CIRCLE ( 'NONE', #7735, 1.120011618224791450 ) ;
#17853=CARTESIAN_POINT ( 'NONE',  ( 18.82264457159015691, 10.97998838177520931, -1.452769935612311825 ) ) ;
#17934=( NAMED_UNIT ( * ) SI_UNIT ( $, .STERADIAN. ) SOLID_ANGLE_UNIT ( ) );
#18000=DIRECTION ( 'NONE',  ( -0.000000000000000000, -0.000000000000000000, -1.000000000000000000 ) ) ;
#18043=CARTESIAN_POINT ( 'NONE',  ( 15.51050023680984680, 10.97998838177520931, 0.05106179917585291356 ) ) ;
#18104=DIRECTION ( 'NONE',  ( -0.000000000000000000, -0.000000000000000000, -1.000000000000000000 ) ) ;
#18141=DIRECTION ( 'NONE',  ( -0.000000000000000000, -0.000000000000000000, -1.000000000000000000 ) ) ;
#18151=LINE ( 'NONE', #6518, #18830 ) ;
#18254=ORIENTED_EDGE ( 'NONE', *, *, #28669, .F. ) ;
#18337=MECHANICAL_DESIGN_GEOMETRIC_PRESENTATION_REPRESENTATION('',(#6275),#7292);
#18410=EDGE_LOOP ( 'NONE', ( #17210, #4642, #11420, #14450 ) ) ;
#18465=( GEOMETRIC_REPRESENTATION_CONTEXT ( 3 ) GLOBAL_UNCERTAINTY_ASSIGNED_CONTEXT ( ( #17569 ) ) GLOBAL_UNIT_ASSIGNED_CONTEXT ( ( #7363, #23747, #12233 ) ) REPRESENTATION_CONTEXT ( 'NONE', 'WORKASPACE' ) );
#18586=DIRECTION ( 'NONE',  ( -1.000000000000000000, 0.000000000000000000, 0.000000000000000000 ) ) ;
#18638=CARTESIAN_POINT ( 'NONE',  ( 17.16657240420000008, 10.97998838177520931, 0.05106179917585291356 ) ) ;
#18830=VECTOR ( 'NONE', #16115, 1000.000000000000114 ) ;
#18887=EDGE_CURVE ( 'NONE', #565, #22567, #11133, .T. ) ;
#19029=FACE_OUTER_BOUND ( 'NONE', #4142, .T. ) ;
#19053=AXIS2_PLACEMENT_3D ( 'NONE', #17685, #881, #8246 ) ;
#19108=DIRECTION ( 'NONE',  ( -1.000000000000000000, 0.000000000000000000, 0.000000000000000000 ) ) ;
#19165=VERTEX_POINT ( 'NONE', #24790 ) ;
#19168=PRESENTATION_STYLE_ASSIGNMENT (( #9247 ) ) ;
#19233=CIRCLE ( 'NONE', #11189, 1.656072167390155281 ) ;
#19316=CIRCLE ( 'NONE', #22324, 1.656072167390155281 ) ;
#19479=SURFACE_SIDE_STYLE ('',( #28919 ) ) ;
#19755=UNCERTAINTY_MEASURE_WITH_UNIT (LENGTH_MEASURE( 1.000000000000000082E-05 ), #17783, 'distance_accuracy_value', 'NONE');
#19810=DIRECTION ( 'NONE',  ( -0.000000000000000000, 0.000000000000000000, -1.000000000000000000 ) ) ;
#19855=COLOUR_RGB ( '', 0.72549020, 0.75294118, 0.79215686) ;
#19906=CARTESIAN_POINT ( 'NONE',  ( 17.16657240420000008, 12.09999999999999964, -1.452769935612311825 ) ) ;
#19912=ORIENTED_EDGE ( 'NONE', *, *, #4741, .T. ) ;
#19969=COLOUR_RGB ( '', 0.72549020, 0.75294118, 0.79215686) ;
#20132=FACE_OUTER_BOUND ( 'NONE', #30509, .T. ) ;
#20150=DIRECTION ( 'NONE',  ( -1.000000000000000000, 0.000000000000000000, 0.000000000000000000 ) ) ;
#20386=EDGE_CURVE ( 'NONE', #22567, #15475, #30697, .T. ) ;
#20543=AXIS2_PLACEMENT_3D ( 'NONE', #16803, #2498, #29073 ) ;
#21175=ADVANCED_BREP_SHAPE_REPRESENTATION ( '', ( #11026, #17722 ), #2272 ) ;
#21177=ORIENTED_EDGE ( 'NONE', *, *, #17106, .F. ) ;
#21300=CIRCLE ( 'NONE', #10729, 1.472846691535505848 ) ;
#21457=CARTESIAN_POINT ( 'NONE',  ( 16.04656078597520974, 10.97998838177520931, -1.452769935612311825 ) ) ;
#21530=ADVANCED_FACE ( 'NONE', ( #12987 ), #9767, .T. ) ;
#21532=CARTESIAN_POINT ( 'NONE',  ( 17.16657240420000008, 10.97998838177520931, -1.972246272986471594 ) ) ;
#21569=EDGE_CURVE ( 'NONE', #27894, #5868, #17789, .T. ) ;
#21721=EDGE_LOOP ( 'NONE', ( #18254, #10771 ) ) ;
#21757=( NAMED_UNIT ( * ) SI_UNIT ( $, .STERADIAN. ) SOLID_ANGLE_UNIT ( ) );
#21996=ORIENTED_EDGE ( 'NONE', *, *, #17377, .F. ) ;
#22038=APPLICATION_CONTEXT ( 'automotive_design' ) ;
#22104=ORIENTED_EDGE ( 'NONE', *, *, #18887, .F. ) ;
#22129=DIRECTION ( 'NONE',  ( -1.000000000000000000, 0.000000000000000000, 0.000000000000000000 ) ) ;
#22181=ADVANCED_FACE ( 'NONE', ( #5939, #3422 ), #27491, .T. ) ;
#22281=DIRECTION ( 'NONE',  ( -1.000000000000000000, 0.000000000000000000, 0.000000000000000000 ) ) ;
#22324=AXIS2_PLACEMENT_3D ( 'NONE', #18638, #4016, #4486 ) ;
#22341=DIRECTION ( 'NONE',  ( -1.000000000000000000, 0.000000000000000000, 0.000000000000000000 ) ) ;
#22352=PRODUCT_DEFINITION ( 'UNKNOWN', '', #10838, #29800 ) ;
#22427=ORIENTED_EDGE ( 'NONE', *, *, #10549, .T. ) ;
#22567=VERTEX_POINT ( 'NONE', #17853 ) ;
#22568=EDGE_LOOP ( 'NONE', ( #24887, #14745 ) ) ;
#22582=VERTEX_POINT ( 'NONE', #2932 ) ;
#22599=DIRECTION ( 'NONE',  ( -0.000000000000000000, -0.000000000000000000, -1.000000000000000000 ) ) ;
#22799=PLANE ( 'NONE',  #2722 ) ;
#22934=CARTESIAN_POINT ( 'NONE',  ( 18.82264457159015691, 10.97998838177520931, 0.05106179917585291356 ) ) ;
#23024=VERTEX_POINT ( 'NONE', #24724 ) ;
#23028=AXIS2_PLACEMENT_3D ( 'NONE', #11800, #26275, #4720 ) ;
#23316=CARTESIAN_POINT ( 'NONE',  ( 17.16657240420000008, 10.97998838177520931, 0.05106179917585291356 ) ) ;
#23747=( NAMED_UNIT ( * ) PLANE_ANGLE_UNIT ( ) SI_UNIT ( $, .RADIAN. ) );
#23837=CARTESIAN_POINT ( 'NONE',  ( 16.04674922903581091, 10.97998838177520931, 0.05106179917585291356 ) ) ;
#24083=EDGE_CURVE ( 'NONE', #19165, #30573, #19316, .T. ) ;
#24161=DIRECTION ( 'NONE',  ( 0.000000000000000000, 0.000000000000000000, 1.000000000000000000 ) ) ;
#24272=ORIENTED_EDGE ( 'NONE', *, *, #29712, .F. ) ;
#24345=CONICAL_SURFACE ( 'NONE', #6261, 1.472846691535505848, 0.3390887027916915653 ) ;
#24724=CARTESIAN_POINT ( 'NONE',  ( 18.63941909573550859, 10.97998838177520931, 0.5194763363741546902 ) ) ;
#24781=EDGE_LOOP ( 'NONE', ( #1246, #19912, #31080, #27088 ) ) ;
#24790=CARTESIAN_POINT ( 'NONE',  ( 18.82264457159015691, 10.97998838177520931, 0.05106179917585291356 ) ) ;
#24887=ORIENTED_EDGE ( 'NONE', *, *, #21569, .T. ) ;
#24961=VERTEX_POINT ( 'NONE', #1585 ) ;
#25096=ORIENTED_EDGE ( 'NONE', *, *, #3346, .T. ) ;
#25105=ADVANCED_FACE ( 'NONE', ( #19029 ), #24345, .T. ) ;
#25291=CIRCLE ( 'NONE', #14246, 1.472846691535505848 ) ;
#25401=DIRECTION ( 'NONE',  ( -1.000000000000000000, 0.000000000000000000, 0.000000000000000000 ) ) ;
#25604=AXIS2_PLACEMENT_3D ( 'NONE', #23316, #18104, #11354 ) ;
#25783=ORIENTED_EDGE ( 'NONE', *, *, #15941, .T. ) ;
#25826=ORIENTED_EDGE ( 'NONE', *, *, #4741, .F. ) ;
#26050=CARTESIAN_POINT ( 'NONE',  ( 17.16657240420000008, 10.97998838177520931, -1.452769935612311825 ) ) ;
#26275=DIRECTION ( 'NONE',  ( -0.000000000000000000, -0.000000000000000000, -1.000000000000000000 ) ) ;
#26475=( LENGTH_UNIT ( ) NAMED_UNIT ( * ) SI_UNIT ( .MILLI., .METRE. ) );
#26611=DIRECTION ( 'NONE',  ( -0.000000000000000000, -0.000000000000000000, -1.000000000000000000 ) ) ;
#26645=LINE ( 'NONE', #74, #26873 ) ;
#26743=ORIENTED_EDGE ( 'NONE', *, *, #17377, .T. ) ;
#26781=FILL_AREA_STYLE ('',( #29137 ) ) ;
#26803=CARTESIAN_POINT ( 'NONE',  ( 17.16657240420000008, 10.97998838177520931, -1.452769935612311825 ) ) ;
#26873=VECTOR ( 'NONE', #5239, 1000.000000000000000 ) ;
#26958=EDGE_CURVE ( 'NONE', #23024, #22582, #21300, .T. ) ;
#27088=ORIENTED_EDGE ( 'NONE', *, *, #10549, .F. ) ;
#27114=AXIS2_PLACEMENT_3D ( 'NONE', #19906, #24161, #16911 ) ;
#27384=DIRECTION ( 'NONE',  ( -0.000000000000000000, -0.000000000000000000, -1.000000000000000000 ) ) ;
#27451=DIRECTION ( 'NONE',  ( -1.000000000000000000, 0.000000000000000000, 0.000000000000000000 ) ) ;
#27491=PLANE ( 'NONE',  #2763 ) ;
#27527=AXIS2_PLACEMENT_3D ( 'NONE', #7919, #18141, #25401 ) ;
#27556=VECTOR ( 'NONE', #13325, 1000.000000000000114 ) ;
#27894=VERTEX_POINT ( 'NONE', #10620 ) ;
#27964=CARTESIAN_POINT ( 'NONE',  ( 18.63941909573550859, 10.97998838177520931, -1.972246272986471594 ) ) ;
#28028=EDGE_LOOP ( 'NONE', ( #5489, #11497 ) ) ;
#28364=EDGE_CURVE ( 'NONE', #10669, #565, #25291, .T. ) ;
#28552=CARTESIAN_POINT ( 'NONE',  ( 17.16657240420000008, 10.97998838177520931, -1.452769935612311825 ) ) ;
#28590=DIRECTION ( 'NONE',  ( -1.000000000000000000, 0.000000000000000000, 0.000000000000000000 ) ) ;
#28669=EDGE_CURVE ( 'NONE', #5834, #24961, #8700, .T. ) ;
#28693=AXIS2_PLACEMENT_3D ( 'NONE', #26050, #4489, #18586 ) ;
#28712=DIRECTION ( 'NONE',  ( -1.000000000000000000, 0.000000000000000000, 0.000000000000000000 ) ) ;
#28735=DIRECTION ( 'NONE',  ( -0.000000000000000000, -0.000000000000000000, -1.000000000000000000 ) ) ;
#28919=SURFACE_STYLE_FILL_AREA ( #3917 ) ;
#29073=DIRECTION ( 'NONE',  ( 1.000000000000000000, 0.000000000000000000, -0.000000000000000000 ) ) ;
#29137=FILL_AREA_STYLE_COLOUR ( '', #19855 ) ;
#29194=CARTESIAN_POINT ( 'NONE',  ( 17.16657240420000008, 10.97998838177520931, -1.452769935612311825 ) ) ;
#29201=ADVANCED_FACE ( 'NONE', ( #10556 ), #30840, .T. ) ;
#29203=DIRECTION ( 'NONE',  ( 1.000000000000000000, 0.000000000000000000, 0.000000000000000000 ) ) ;
#29285=CONICAL_SURFACE ( 'NONE', #3653, 1.120011618224791450, 0.0001253086068439055573 ) ;
#29604=( NAMED_UNIT ( * ) PLANE_ANGLE_UNIT ( ) SI_UNIT ( $, .RADIAN. ) );
#29712=EDGE_CURVE ( 'NONE', #22582, #30573, #8443, .T. ) ;
#29742=CARTESIAN_POINT ( 'NONE',  ( 17.16657240420000008, 10.97998838177520931, -1.452769935612311825 ) ) ;
#29800=PRODUCT_DEFINITION_CONTEXT ( 'detailed design', #22038, 'design' ) ;
#30189=FILL_AREA_STYLE_COLOUR ( '', #19969 ) ;
#30509=EDGE_LOOP ( 'NONE', ( #9356, #15155 ) ) ;
#30511=PRODUCT ( 'Rivet', 'Rivet', '', ( #17447 ) ) ;
#30573=VERTEX_POINT ( 'NONE', #2590 ) ;
#30697=CIRCLE ( 'NONE', #28693, 1.656072167390155281 ) ;
#30840=CONICAL_SURFACE ( 'NONE', #3200, 1.120011618224791450, 0.0001253086068439055573 ) ;
#31080=ORIENTED_EDGE ( 'NONE', *, *, #21569, .F. ) ;
#31081=DIRECTION ( 'NONE',  ( -0.000000000000000000, -0.000000000000000000, -1.000000000000000000 ) ) ;
ENDSEC;
END-ISO-10303-21;
